ISO-10303-21;
HEADER;
/* Generated by software containing ST-Developer
 * from STEP Tools, Inc. (www.steptools.com) 
 */

FILE_DESCRIPTION(
/* description */ ('PAT-072'),
/* implementation_level */ '2;1');

FILE_NAME(
/* name */ 'M2 sight screw (3).step',
/* time_stamp */ '2026-10-29T20:11:56-07:00',
/* author */ (''),
/* organization */ (''),
/* preprocessor_version */ 'ST-DEVELOPER v20.2',
/* originating_system */ 'Autodesk Translation Framework v15.17.0.0',
/* authorisation */ '');

FILE_SCHEMA (('AUTOMOTIVE_DESIGN { 1 0 10303 214 3 1 1 }'));
ENDSEC;

DATA;
#10=MECHANICAL_DESIGN_GEOMETRIC_PRESENTATION_REPRESENTATION('',(#357),#11432);
#285=SHAPE_REPRESENTATION_RELATIONSHIP('SRR','None',#11589,#321);
#321=ADVANCED_BREP_SHAPE_REPRESENTATION('',(#393),#11420);
#357=STYLED_ITEM('',(#11826),#393);
#393=MANIFOLD_SOLID_BREP('Body1',#6092);
#531=FACE_BOUND('',#1561,.T.);
#723=PLANE('',#7007);
#724=PLANE('',#7008);
#725=PLANE('',#7009);
#726=PLANE('',#7012);
#727=PLANE('',#7014);
#728=PLANE('',#7017);
#729=PLANE('',#7023);
#1054=FACE_OUTER_BOUND('',#1555,.T.);
#1055=FACE_OUTER_BOUND('',#1556,.T.);
#1056=FACE_OUTER_BOUND('',#1557,.T.);
#1057=FACE_OUTER_BOUND('',#1558,.T.);
#1058=FACE_OUTER_BOUND('',#1559,.T.);
#1059=FACE_OUTER_BOUND('',#1560,.T.);
#1060=FACE_OUTER_BOUND('',#1562,.T.);
#1061=FACE_OUTER_BOUND('',#1563,.T.);
#1062=FACE_OUTER_BOUND('',#1564,.T.);
#1555=EDGE_LOOP('',(#5114,#5115,#5116,#5117));
#1556=EDGE_LOOP('',(#5118,#5119,#5120,#5121));
#1557=EDGE_LOOP('',(#5122,#5123,#5124,#5125));
#1558=EDGE_LOOP('',(#5126,#5127));
#1559=EDGE_LOOP('',(#5128,#5129,#5130));
#1560=EDGE_LOOP('',(#5131));
#1561=EDGE_LOOP('',(#5132));
#1562=EDGE_LOOP('',(#5133,#5134,#5135,#5136,#5137,#5138,#5139,#5140,#5141,
#5142,#5143,#5144));
#1563=EDGE_LOOP('',(#5145,#5146,#5147,#5148));
#1564=EDGE_LOOP('',(#5149));
#1982=LINE('',#10816,#2401);
#1983=LINE('',#10818,#2402);
#1984=LINE('',#10820,#2403);
#1985=LINE('',#10821,#2404);
#1986=LINE('',#10825,#2405);
#1987=LINE('',#10827,#2406);
#1988=LINE('',#10829,#2407);
#1989=LINE('',#10830,#2408);
#1990=LINE('',#10846,#2409);
#1991=LINE('',#10850,#2410);
#2401=VECTOR('',#8545,1.);
#2402=VECTOR('',#8546,1.);
#2403=VECTOR('',#8547,1.);
#2404=VECTOR('',#8548,1.);
#2405=VECTOR('',#8551,1.);
#2406=VECTOR('',#8552,1.);
#2407=VECTOR('',#8553,1.);
#2408=VECTOR('',#8554,1.);
#2409=VECTOR('',#8579,0.175);
#2410=VECTOR('',#8584,0.1);
#2759=CIRCLE('',#7010,0.175);
#2760=CIRCLE('',#7011,0.175);
#2761=CIRCLE('',#7013,0.175);
#2762=CIRCLE('',#7015,0.175);
#2763=CIRCLE('',#7016,0.175);
#2764=CIRCLE('',#7018,0.175);
#2765=CIRCLE('',#7019,0.1);
#2766=CIRCLE('',#7022,0.1);
#3178=VERTEX_POINT('',#10814);
#3179=VERTEX_POINT('',#10815);
#3180=VERTEX_POINT('',#10817);
#3181=VERTEX_POINT('',#10819);
#3182=VERTEX_POINT('',#10823);
#3183=VERTEX_POINT('',#10824);
#3184=VERTEX_POINT('',#10826);
#3185=VERTEX_POINT('',#10828);
#3186=VERTEX_POINT('',#10837);
#3187=VERTEX_POINT('',#10841);
#3188=VERTEX_POINT('',#10843);
#3189=VERTEX_POINT('',#10848);
#3846=EDGE_CURVE('',#3178,#3179,#1982,.T.);
#3847=EDGE_CURVE('',#3178,#3180,#1983,.T.);
#3848=EDGE_CURVE('',#3181,#3180,#1984,.T.);
#3849=EDGE_CURVE('',#3179,#3181,#1985,.T.);
#3850=EDGE_CURVE('',#3182,#3183,#1986,.T.);
#3851=EDGE_CURVE('',#3184,#3182,#1987,.T.);
#3852=EDGE_CURVE('',#3185,#3184,#1988,.T.);
#3853=EDGE_CURVE('',#3185,#3183,#1989,.T.);
#3854=EDGE_CURVE('',#3183,#3178,#2759,.T.);
#3855=EDGE_CURVE('',#3180,#3185,#2760,.T.);
#3856=EDGE_CURVE('',#3184,#3182,#2761,.T.);
#3857=EDGE_CURVE('',#3186,#3181,#2762,.T.);
#3858=EDGE_CURVE('',#3179,#3186,#2763,.T.);
#3859=EDGE_CURVE('',#3187,#3187,#2764,.T.);
#3860=EDGE_CURVE('',#3188,#3188,#2765,.T.);
#3861=EDGE_CURVE('',#3187,#3186,#1990,.T.);
#3862=EDGE_CURVE('',#3189,#3189,#2766,.T.);
#3863=EDGE_CURVE('',#3189,#3188,#1991,.T.);
#5114=ORIENTED_EDGE('',*,*,#3846,.F.);
#5115=ORIENTED_EDGE('',*,*,#3847,.T.);
#5116=ORIENTED_EDGE('',*,*,#3848,.F.);
#5117=ORIENTED_EDGE('',*,*,#3849,.F.);
#5118=ORIENTED_EDGE('',*,*,#3850,.F.);
#5119=ORIENTED_EDGE('',*,*,#3851,.F.);
#5120=ORIENTED_EDGE('',*,*,#3852,.F.);
#5121=ORIENTED_EDGE('',*,*,#3853,.T.);
#5122=ORIENTED_EDGE('',*,*,#3854,.F.);
#5123=ORIENTED_EDGE('',*,*,#3853,.F.);
#5124=ORIENTED_EDGE('',*,*,#3855,.F.);
#5125=ORIENTED_EDGE('',*,*,#3847,.F.);
#5126=ORIENTED_EDGE('',*,*,#3851,.T.);
#5127=ORIENTED_EDGE('',*,*,#3856,.F.);
#5128=ORIENTED_EDGE('',*,*,#3849,.T.);
#5129=ORIENTED_EDGE('',*,*,#3857,.F.);
#5130=ORIENTED_EDGE('',*,*,#3858,.F.);
#5131=ORIENTED_EDGE('',*,*,#3859,.T.);
#5132=ORIENTED_EDGE('',*,*,#3860,.F.);
#5133=ORIENTED_EDGE('',*,*,#3859,.F.);
#5134=ORIENTED_EDGE('',*,*,#3861,.T.);
#5135=ORIENTED_EDGE('',*,*,#3857,.T.);
#5136=ORIENTED_EDGE('',*,*,#3848,.T.);
#5137=ORIENTED_EDGE('',*,*,#3855,.T.);
#5138=ORIENTED_EDGE('',*,*,#3852,.T.);
#5139=ORIENTED_EDGE('',*,*,#3856,.T.);
#5140=ORIENTED_EDGE('',*,*,#3850,.T.);
#5141=ORIENTED_EDGE('',*,*,#3854,.T.);
#5142=ORIENTED_EDGE('',*,*,#3846,.T.);
#5143=ORIENTED_EDGE('',*,*,#3858,.T.);
#5144=ORIENTED_EDGE('',*,*,#3861,.F.);
#5145=ORIENTED_EDGE('',*,*,#3862,.F.);
#5146=ORIENTED_EDGE('',*,*,#3863,.T.);
#5147=ORIENTED_EDGE('',*,*,#3860,.T.);
#5148=ORIENTED_EDGE('',*,*,#3863,.F.);
#5149=ORIENTED_EDGE('',*,*,#3862,.T.);
#5663=CYLINDRICAL_SURFACE('',#7020,0.175);
#5664=CYLINDRICAL_SURFACE('',#7021,0.1);
#5953=ADVANCED_FACE('',(#1054),#723,.F.);
#5954=ADVANCED_FACE('',(#1055),#724,.F.);
#5955=ADVANCED_FACE('',(#1056),#725,.F.);
#5956=ADVANCED_FACE('',(#1057),#726,.F.);
#5957=ADVANCED_FACE('',(#1058),#727,.F.);
#5958=ADVANCED_FACE('',(#1059,#531),#728,.T.);
#5959=ADVANCED_FACE('',(#1060),#5663,.T.);
#5960=ADVANCED_FACE('',(#1061),#5664,.T.);
#5961=ADVANCED_FACE('',(#1062),#729,.T.);
#6092=CLOSED_SHELL('',(#5953,#5954,#5955,#5956,#5957,#5958,#5959,#5960,
#5961));
#7006=AXIS2_PLACEMENT_3D('',#10812,#8541,#8542);
#7007=AXIS2_PLACEMENT_3D('',#10813,#8543,#8544);
#7008=AXIS2_PLACEMENT_3D('',#10822,#8549,#8550);
#7009=AXIS2_PLACEMENT_3D('',#10831,#8555,#8556);
#7010=AXIS2_PLACEMENT_3D('',#10832,#8557,#8558);
#7011=AXIS2_PLACEMENT_3D('',#10833,#8559,#8560);
#7012=AXIS2_PLACEMENT_3D('',#10834,#8561,#8562);
#7013=AXIS2_PLACEMENT_3D('',#10835,#8563,#8564);
#7014=AXIS2_PLACEMENT_3D('',#10836,#8565,#8566);
#7015=AXIS2_PLACEMENT_3D('',#10838,#8567,#8568);
#7016=AXIS2_PLACEMENT_3D('',#10839,#8569,#8570);
#7017=AXIS2_PLACEMENT_3D('',#10840,#8571,#8572);
#7018=AXIS2_PLACEMENT_3D('',#10842,#8573,#8574);
#7019=AXIS2_PLACEMENT_3D('',#10844,#8575,#8576);
#7020=AXIS2_PLACEMENT_3D('',#10845,#8577,#8578);
#7021=AXIS2_PLACEMENT_3D('',#10847,#8580,#8581);
#7022=AXIS2_PLACEMENT_3D('',#10849,#8582,#8583);
#7023=AXIS2_PLACEMENT_3D('',#10851,#8585,#8586);
#8541=DIRECTION('axis',(0.,0.,1.));
#8542=DIRECTION('refdir',(1.,0.,0.));
#8543=DIRECTION('center_axis',(-1.,0.,0.));
#8544=DIRECTION('ref_axis',(0.,0.,1.));
#8545=DIRECTION('',(0.,-1.,0.));
#8546=DIRECTION('',(0.,0.,1.));
#8547=DIRECTION('',(0.,1.,0.));
#8548=DIRECTION('',(0.,0.,1.));
#8549=DIRECTION('center_axis',(1.,0.,0.));
#8550=DIRECTION('ref_axis',(0.,0.,-1.));
#8551=DIRECTION('',(0.,1.,0.));
#8552=DIRECTION('',(0.,0.,-1.));
#8553=DIRECTION('',(0.,-1.,0.));
#8554=DIRECTION('',(0.,0.,-1.));
#8555=DIRECTION('center_axis',(0.,1.,0.));
#8556=DIRECTION('ref_axis',(0.,0.,1.));
#8557=DIRECTION('center_axis',(0.,1.,0.));
#8558=DIRECTION('ref_axis',(1.,0.,0.));
#8559=DIRECTION('center_axis',(0.,1.,0.));
#8560=DIRECTION('ref_axis',(1.,0.,0.));
#8561=DIRECTION('center_axis',(0.,1.,0.));
#8562=DIRECTION('ref_axis',(1.,0.,0.));
#8563=DIRECTION('center_axis',(0.,1.,0.));
#8564=DIRECTION('ref_axis',(1.,0.,0.));
#8565=DIRECTION('center_axis',(0.,1.,0.));
#8566=DIRECTION('ref_axis',(1.,0.,0.));
#8567=DIRECTION('center_axis',(0.,1.,0.));
#8568=DIRECTION('ref_axis',(1.,0.,0.));
#8569=DIRECTION('center_axis',(0.,1.,0.));
#8570=DIRECTION('ref_axis',(1.,0.,0.));
#8571=DIRECTION('center_axis',(0.,1.,0.));
#8572=DIRECTION('ref_axis',(1.,0.,0.));
#8573=DIRECTION('center_axis',(0.,1.,0.));
#8574=DIRECTION('ref_axis',(1.,0.,0.));
#8575=DIRECTION('center_axis',(0.,1.,0.));
#8576=DIRECTION('ref_axis',(1.,0.,0.));
#8577=DIRECTION('center_axis',(0.,1.,0.));
#8578=DIRECTION('ref_axis',(1.,0.,0.));
#8579=DIRECTION('',(0.,-1.,0.));
#8580=DIRECTION('center_axis',(0.,1.,0.));
#8581=DIRECTION('ref_axis',(1.,0.,0.));
#8582=DIRECTION('center_axis',(0.,1.,0.));
#8583=DIRECTION('ref_axis',(1.,0.,0.));
#8584=DIRECTION('',(0.,-1.,0.));
#8585=DIRECTION('center_axis',(0.,1.,0.));
#8586=DIRECTION('ref_axis',(1.,0.,0.));
#10812=CARTESIAN_POINT('',(0.,0.,0.));
#10813=CARTESIAN_POINT('Origin',(0.77,-3.4,13.));
#10814=CARTESIAN_POINT('',(0.77,-3.2,13.0275906035043));
#10815=CARTESIAN_POINT('',(0.77,-3.3,13.0275906035043));
#10816=CARTESIAN_POINT('',(0.77,-3.3,13.0275906035043));
#10817=CARTESIAN_POINT('',(0.77,-3.2,13.3724093964957));
#10818=CARTESIAN_POINT('',(0.77,-3.2,13.4));
#10819=CARTESIAN_POINT('',(0.77,-3.3,13.3724093964957));
#10820=CARTESIAN_POINT('',(0.77,-3.3,13.3724093964957));
#10821=CARTESIAN_POINT('',(0.77,-3.3,13.1));
#10822=CARTESIAN_POINT('Origin',(0.83,-3.4,13.4));
#10823=CARTESIAN_POINT('',(0.83,-3.3,13.0275906035043));
#10824=CARTESIAN_POINT('',(0.83,-3.2,13.0275906035043));
#10825=CARTESIAN_POINT('',(0.83,-3.3,13.0275906035043));
#10826=CARTESIAN_POINT('',(0.83,-3.3,13.3724093964957));
#10827=CARTESIAN_POINT('',(0.83,-3.3,13.3));
#10828=CARTESIAN_POINT('',(0.83,-3.2,13.3724093964957));
#10829=CARTESIAN_POINT('',(0.83,-3.3,13.3724093964957));
#10830=CARTESIAN_POINT('',(0.83,-3.2,13.));
#10831=CARTESIAN_POINT('Origin',(0.8,-3.2,13.2));
#10832=CARTESIAN_POINT('Origin',(0.8,-3.2,13.2));
#10833=CARTESIAN_POINT('Origin',(0.8,-3.2,13.2));
#10834=CARTESIAN_POINT('Origin',(0.8,-3.3,13.2));
#10835=CARTESIAN_POINT('Origin',(0.8,-3.3,13.2));
#10836=CARTESIAN_POINT('Origin',(0.8,-3.3,13.2));
#10837=CARTESIAN_POINT('',(0.625,-3.3,13.2));
#10838=CARTESIAN_POINT('Origin',(0.8,-3.3,13.2));
#10839=CARTESIAN_POINT('Origin',(0.8,-3.3,13.2));
#10840=CARTESIAN_POINT('Origin',(0.8,-3.1,13.2));
#10841=CARTESIAN_POINT('',(0.625,-3.1,13.2));
#10842=CARTESIAN_POINT('Origin',(0.8,-3.1,13.2));
#10843=CARTESIAN_POINT('',(0.7,-3.1,13.2));
#10844=CARTESIAN_POINT('Origin',(0.8,-3.1,13.2));
#10845=CARTESIAN_POINT('Origin',(0.8,-3.3,13.2));
#10846=CARTESIAN_POINT('',(0.625,-3.3,13.2));
#10847=CARTESIAN_POINT('Origin',(0.8,-3.1,13.2));
#10848=CARTESIAN_POINT('',(0.7,-2.1,13.2));
#10849=CARTESIAN_POINT('Origin',(0.8,-2.1,13.2));
#10850=CARTESIAN_POINT('',(0.7,-3.1,13.2));
#10851=CARTESIAN_POINT('Origin',(0.8,-2.1,13.2));
#11381=UNCERTAINTY_MEASURE_WITH_UNIT(LENGTH_MEASURE(0.001),#11433,
'DISTANCE_ACCURACY_VALUE',
'Maximum model space distance between geometric entities at asserted c
onnectivities');
#11393=UNCERTAINTY_MEASURE_WITH_UNIT(LENGTH_MEASURE(0.001),#11433,
'DISTANCE_ACCURACY_VALUE',
'Maximum model space distance between geometric entities at asserted c
onnectivities');
#11420=(
GEOMETRIC_REPRESENTATION_CONTEXT(3)
GLOBAL_UNCERTAINTY_ASSIGNED_CONTEXT((#11381))
GLOBAL_UNIT_ASSIGNED_CONTEXT((#11433,#11435,#11436))
REPRESENTATION_CONTEXT('','3D')
);
#11432=(
GEOMETRIC_REPRESENTATION_CONTEXT(3)
GLOBAL_UNCERTAINTY_ASSIGNED_CONTEXT((#11393))
GLOBAL_UNIT_ASSIGNED_CONTEXT((#11433,#11435,#11436))
REPRESENTATION_CONTEXT('','3D')
);
#11433=(
LENGTH_UNIT()
NAMED_UNIT(*)
SI_UNIT(.CENTI.,.METRE.)
);
#11435=(
NAMED_UNIT(*)
PLANE_ANGLE_UNIT()
SI_UNIT($,.RADIAN.)
);
#11436=(
NAMED_UNIT(*)
SI_UNIT($,.STERADIAN.)
SOLID_ANGLE_UNIT()
);
#11463=SHAPE_DEFINITION_REPRESENTATION(#11501,#11589);
#11501=PRODUCT_DEFINITION_SHAPE('',$,#11628);
#11589=SHAPE_REPRESENTATION('',(#7006),#11420);
#11601=PRODUCT_DEFINITION_CONTEXT('part definition',#11717,'design');
#11628=PRODUCT_DEFINITION('M2 sight screw (3)',
'M2 sight screw (3)',#11666,#11601);
#11666=PRODUCT_DEFINITION_FORMATION('',$,#11745);
#11717=APPLICATION_CONTEXT(
'Core Data for Automotive Mechanical Design Process');
#11718=PRODUCT_CONTEXT('part definition',#11717,'mechanical');
#11745=PRODUCT('M2 sight screw (3)','M2 sight screw (3)',
'M2 sight screw (3)',(#11718));
#11820=COLOUR_RGB('Black',0.12,0.14,0.17);
#11821=FILL_AREA_STYLE_COLOUR('',#11820);
#11822=FILL_AREA_STYLE('',(#11821));
#11823=SURFACE_STYLE_FILL_AREA(#11822);
#11824=SURFACE_SIDE_STYLE('',(#11823));
#11825=SURFACE_STYLE_USAGE(.BOTH.,#11824);
#11826=PRESENTATION_STYLE_ASSIGNMENT((#11825));
ENDSEC;
END-ISO-10303-21;
